ISO-10303-21;
HEADER;
FILE_DESCRIPTION (('STEP AP214'),
    '1' );
FILE_NAME ('pulley screw_short.step',
    '2026-10-12T23:53:07',
    ( '' ),
    ( '' ),
    'SwSTEP 2.0',
    'SolidWorks 2024',
    '' );
FILE_SCHEMA (( 'AUTOMOTIVE_DESIGN' ));
ENDSEC;

DATA;
#8=EDGE_LOOP ( 'NONE', ( #25751, #37385, #3783, #18392 ) ) ;
#71=DIRECTION ( 'NONE',  ( 2.465190328815661892E-32, 1.000000000000000000, -5.978086547377980964E-31 ) ) ;
#74=PLANE ( 'NONE',  #31747 ) ;
#143=EDGE_CURVE ( 'NONE', #32215, #37335, #22584, .T. ) ;
#176=CARTESIAN_POINT ( 'NONE',  ( 0.09624682736800391214, 0.06028806207340059453, 0.08329560493130624965 ) ) ;
#433=VERTEX_POINT ( 'NONE', #39601 ) ;
#688=ORIENTED_EDGE ( 'NONE', *, *, #21311, .T. ) ;
#776=CARTESIAN_POINT ( 'NONE',  ( 0.000000000000000000, 0.08637707520836798714, 0.000000000000000000 ) ) ;
#898=ORIENTED_EDGE ( 'NONE', *, *, #29268, .T. ) ;
#986=PLANE ( 'NONE',  #27207 ) ;
#1019=ORIENTED_EDGE ( 'NONE', *, *, #18787, .T. ) ;
#1055=CARTESIAN_POINT ( 'NONE',  ( 0.07216878364870175921, 0.000000000000000000, -0.1249999999999971689 ) ) ;
#1100=ORIENTED_EDGE ( 'NONE', *, *, #3166, .F. ) ;
#1126=( CONVERSION_BASED_UNIT ( 'INCH', #10967 ) LENGTH_UNIT ( ) NAMED_UNIT ( #23398 ) );
#1156=EDGE_CURVE ( 'NONE', #433, #25927, #7747, .T. ) ;
#1238=ORIENTED_EDGE ( 'NONE', *, *, #7385, .F. ) ;
#1248=CARTESIAN_POINT ( 'NONE',  ( -1.502516396515344672E-15, -0.3899999999999999578, 5.463695987328526437E-16 ) ) ;
#1355=CARTESIAN_POINT ( 'NONE',  ( 0.07216878364870298046, 0.08000000000000023759, -0.1249999999999999029 ) ) ;
#1366=ORIENTED_EDGE ( 'NONE', *, *, #1156, .T. ) ;
#1428=ORIENTED_EDGE ( 'NONE', *, *, #23324, .T. ) ;
#1500=DIRECTION ( 'NONE',  ( 1.000000000000000000, 9.860761315262660705E-32, 5.551115123125790098E-17 ) ) ;
#1515=CARTESIAN_POINT ( 'NONE',  ( 0.07216878364870311924, 0.000000000000000000, 0.1249999999999999029 ) ) ;
#1654=ORIENTED_EDGE ( 'NONE', *, *, #30058, .T. ) ;
#1901=CARTESIAN_POINT ( 'NONE',  ( 0.000000000000000000, 0.000000000000000000, 0.000000000000000000 ) ) ;
#2077=DIRECTION ( 'NONE',  ( 0.000000000000000000, 0.000000000000000000, 1.000000000000000000 ) ) ;
#2098=EDGE_CURVE ( 'NONE', #433, #19840, #12446, .T. ) ;
#2205=EDGE_CURVE ( 'NONE', #8583, #9507, #4541, .T. ) ;
#2229=ORIENTED_EDGE ( 'NONE', *, *, #14727, .F. ) ;
#2435=EDGE_CURVE ( 'NONE', #37335, #8583, #13370, .T. ) ;
#2477=ORIENTED_EDGE ( 'NONE', *, *, #28253, .T. ) ;
#2599=CARTESIAN_POINT ( 'NONE',  ( -0.1443375672974067936, 0.000000000000000000, 0.000000000000000000 ) ) ;
#2704=LENGTH_MEASURE_WITH_UNIT ( LENGTH_MEASURE( 0.02539999999999999897 ), #18340 );
#2781=CARTESIAN_POINT ( 'NONE',  ( -0.1141309172362121732, 0.06118878220587060240, 0.05231945263244267008 ) ) ;
#2813=CARTESIAN_POINT ( 'NONE',  ( 0.07216878364870311924, 0.05141091571461162829, 0.1249999999999999029 ) ) ;
#2849=CARTESIAN_POINT ( 'NONE',  ( 0.000000000000000000, -0.4700000000000001954, 0.000000000000000000 ) ) ;
#2921=CARTESIAN_POINT ( 'NONE',  ( -0.07216878364870325802, 0.05141091571461162829, -0.1249999999999999029 ) ) ;
#2961=DIRECTION ( 'NONE',  ( 0.000000000000000000, 0.000000000000000000, 1.000000000000000000 ) ) ;
#3029=CARTESIAN_POINT ( 'NONE',  ( 0.1205378779716006349, 0.06113703066755019067, 0.04122227111665002081 ) ) ;
#3166=EDGE_CURVE ( 'NONE', #22246, #37335, #7888, .T. ) ;
#3328=EDGE_CURVE ( 'NONE', #35047, #21906, #30730, .T. ) ;
#3358=AXIS2_PLACEMENT_3D ( 'NONE', #17795, #24201, #36725 ) ;
#3360=CARTESIAN_POINT ( 'NONE',  ( -0.1205378779716004267, 0.06113703066755032944, -0.04122227111665026367 ) ) ;
#3404=PLANE ( 'NONE',  #40456 ) ;
#3407=EDGE_CURVE ( 'NONE', #25927, #37283, #33816, .T. ) ;
#3517=PLANE ( 'NONE',  #36506 ) ;
#3537=ORIENTED_EDGE ( 'NONE', *, *, #143, .T. ) ;
#3574=CARTESIAN_POINT ( 'NONE',  ( -0.1324860366999176253, 0.05739311687334418960, -0.02052745314230725732 ) ) ;
#3697=ORIENTED_EDGE ( 'NONE', *, *, #2435, .F. ) ;
#3783=ORIENTED_EDGE ( 'NONE', *, *, #7385, .T. ) ;
#3882=LINE ( 'NONE', #1055, #23921 ) ;
#3931=VERTEX_POINT ( 'NONE', #6942 ) ;
#4000=DIRECTION ( 'NONE',  ( 0.000000000000000000, -5.978086547377980964E-31, -1.000000000000000000 ) ) ;
#4122=ORIENTED_EDGE ( 'NONE', *, *, #25359, .F. ) ;
#4285=VERTEX_POINT ( 'NONE', #5465 ) ;
#4325=PRODUCT_DEFINITION_CONTEXT ( 'detailed design', #6889, 'design' ) ;
#4476=ADVANCED_FACE ( 'NONE', ( #12656 ), #3404, .T. ) ;
#4541=LINE ( 'NONE', #14412, #15219 ) ;
#4568=ORIENTED_EDGE ( 'NONE', *, *, #29268, .F. ) ;
#4664=ORIENTED_EDGE ( 'NONE', *, *, #19793, .F. ) ;
#4826=CARTESIAN_POINT ( 'NONE',  ( 0.1443375672974070711, 0.05141091571461162829, 0.000000000000000000 ) ) ;
#4873=CARTESIAN_POINT ( 'NONE',  ( -1.496393162519624559E-15, 3.328006943901148699E-32, -0.05000000000000002359 ) ) ;
#4910=VECTOR ( 'NONE', #32991, 39.37007874015748143 ) ;
#5239=CARTESIAN_POINT ( 'NONE',  ( -0.1443375672974067936, 0.05141091571461216952, 0.000000000000000000 ) ) ;
#5327=ORIENTED_EDGE ( 'NONE', *, *, #2098, .T. ) ;
#5465=CARTESIAN_POINT ( 'NONE',  ( 1.530770926392632502E-17, 0.06117178301711245075, 0.1249999999999993477 ) ) ;
#5623=DIRECTION ( 'NONE',  ( 2.465190328815661892E-32, 1.000000000000000000, 6.656013887802287108E-31 ) ) ;
#5729=DIRECTION ( 'NONE',  ( -2.465190328815661892E-32, -1.000000000000000000, -6.656013887802287108E-31 ) ) ;
#5733=CARTESIAN_POINT ( 'NONE',  ( -0.06034227824829735409, 0.05439570041090503044, 0.1249999999999993477 ) ) ;
#5957=DIRECTION ( 'NONE',  ( 0.000000000000000000, 5.978086547377980964E-31, 1.000000000000000000 ) ) ;
#6030=AXIS2_PLACEMENT_3D ( 'NONE', #40417, #9134, #21700 ) ;
#6050=CARTESIAN_POINT ( 'NONE',  ( -0.1202595235781067778, 0.06028806207340019208, 0.04170439506869236951 ) ) ;
#6224=AXIS2_PLACEMENT_3D ( 'NONE', #18857, #18029, #18237 ) ;
#6242=VECTOR ( 'NONE', #9549, 39.37007874015748143 ) ;
#6269=ORIENTED_EDGE ( 'NONE', *, *, #2435, .T. ) ;
#6339=CARTESIAN_POINT ( 'NONE',  ( 1.530770926392632502E-17, 0.06117178301711245075, 0.1249999999999993477 ) ) ;
#6408=EDGE_CURVE ( 'NONE', #8492, #25716, #18287, .T. ) ;
#6514=CARTESIAN_POINT ( 'NONE',  ( 4.898587196579362494E-18, -0.3899999999999999578, -0.03999999999999947348 ) ) ;
#6662=ORIENTED_EDGE ( 'NONE', *, *, #12452, .F. ) ;
#6664=EDGE_LOOP ( 'NONE', ( #9055, #3697, #9148, #26214, #9021, #23750 ) ) ;
#6667=CARTESIAN_POINT ( 'NONE',  ( -0.1443375672974067936, 0.05141091571461216952, 0.000000000000000000 ) ) ;
#6677=AXIS2_PLACEMENT_3D ( 'NONE', #7276, #26439, #29716 ) ;
#6888=DIRECTION ( 'NONE',  ( -2.465190328815661892E-32, -1.000000000000000000, 5.978086547377980964E-31 ) ) ;
#6889=APPLICATION_CONTEXT ( 'configuration controlled 3d designs of mechanical parts and assemblies' ) ;
#6942=CARTESIAN_POINT ( 'NONE',  ( 0.1443375672974070711, 0.000000000000000000, 0.000000000000000000 ) ) ;
#7276=CARTESIAN_POINT ( 'NONE',  ( 0.000000000000000000, -0.4700000000000001954, 0.000000000000000000 ) ) ;
#7385=EDGE_CURVE ( 'NONE', #38442, #13009, #24972, .T. ) ;
#7455=CYLINDRICAL_SURFACE ( 'NONE', #33577, 0.04000000000000000777 ) ;
#7554=EDGE_CURVE ( 'NONE', #17499, #4285, #15288, .T. ) ;
#7680=CARTESIAN_POINT ( 'NONE',  ( 0.07216878364870175921, 0.05141091571461216952, -0.1249999999999971689 ) ) ;
#7708=EDGE_CURVE ( 'NONE', #28983, #8492, #17885, .T. ) ;
#7747=CIRCLE ( 'NONE', #13672, 0.05000000000000000971 ) ;
#7796=FACE_OUTER_BOUND ( 'NONE', #8, .T. ) ;
#7888=LINE ( 'NONE', #23759, #4910 ) ;
#7941=AXIS2_PLACEMENT_3D ( 'NONE', #1901, #35625, #35836 ) ;
#7990=CYLINDRICAL_SURFACE ( 'NONE', #24462, 0.04000000000000000777 ) ;
#8023=ORIENTED_EDGE ( 'NONE', *, *, #22549, .T. ) ;
#8315=DIRECTION ( 'NONE',  ( 1.000000000000000000, 0.000000000000000000, 0.000000000000000000 ) ) ;
#8331=DIRECTION ( 'NONE',  ( 2.465190328815661892E-32, 1.000000000000000000, 6.656013887802287108E-31 ) ) ;
#8429=DIRECTION ( 'NONE',  ( -1.110842377313538251E-32, -0.4506112020353472136, -0.8927203059190820245 ) ) ;
#8441=FACE_BOUND ( 'NONE', #27390, .T. ) ;
#8492=VERTEX_POINT ( 'NONE', #12088 ) ;
#8583=VERTEX_POINT ( 'NONE', #37570 ) ;
#8615=B_SPLINE_CURVE_WITH_KNOTS ( 'NONE', 3,
 ( #31597, #34883, #3029, #12077, #176, #18246, #12467, #2813 ),
 .UNSPECIFIED., .F., .F.,
 ( 4, 2, 2, 4 ),
 ( 2.350980519172206433E-07, 0.001838925622864722624, 0.002758270885271125235, 0.003677616147677528063 ),
 .UNSPECIFIED. ) ;
#8765=DIRECTION ( 'NONE',  ( 0.5000000000000000000, -4.252453317207019391E-31, -0.8660254037844384856 ) ) ;
#8811=VERTEX_POINT ( 'NONE', #4826 ) ;
#8870=AXIS2_PLACEMENT_3D ( 'NONE', #27910, #12067, #8765 ) ;
#8920=CARTESIAN_POINT ( 'NONE',  ( 0.000000000000000000, 0.000000000000000000, 0.000000000000000000 ) ) ;
#8974=FACE_OUTER_BOUND ( 'NONE', #28663, .T. ) ;
#9021=ORIENTED_EDGE ( 'NONE', *, *, #24785, .F. ) ;
#9055=ORIENTED_EDGE ( 'NONE', *, *, #2205, .F. ) ;
#9124=ADVANCED_FACE ( 'NONE', ( #39818 ), #18406, .T. ) ;
#9134=DIRECTION ( 'NONE',  ( 2.465190328815661892E-32, 1.000000000000000000, 6.656013887802287108E-31 ) ) ;
#9148=ORIENTED_EDGE ( 'NONE', *, *, #143, .F. ) ;
#9329=DIRECTION ( 'NONE',  ( 2.465190328815661892E-32, 1.000000000000000000, 6.656013887802287108E-31 ) ) ;
#9434=ADVANCED_FACE ( 'NONE', ( #15891 ), #28435, .F. ) ;
#9481=CARTESIAN_POINT ( 'NONE',  ( 0.07216878364870311924, 0.08000000000000023759, 0.1249999999999999029 ) ) ;
#9502=DIRECTION ( 'NONE',  ( -0.5000000000000003331, -6.162975822039154730E-31, -0.8660254037844383745 ) ) ;
#9507=VERTEX_POINT ( 'NONE', #31127 ) ;
#9549=DIRECTION ( 'NONE',  ( -2.465190328815661892E-32, -1.000000000000000000, -6.656013887802287108E-31 ) ) ;
#9601=CARTESIAN_POINT ( 'NONE',  ( -1.502516396515344672E-15, -0.3899999999999999578, 0.04000000000000055594 ) ) ;
#9733=EDGE_CURVE ( 'NONE', #28983, #23947, #38223, .T. ) ;
#9881=B_SPLINE_CURVE_WITH_KNOTS ( 'NONE', 3,
 ( #31754, #3574, #3360, #16742, #29070, #19014, #16142, #35442 ),
 .UNSPECIFIED., .F., .F.,
 ( 4, 2, 2, 4 ),
 ( 2.350980519117237965E-07, 0.001838925622864737370, 0.002758270885271150389, 0.003677616147677563625 ),
 .UNSPECIFIED. ) ;
#10079=ORIENTED_EDGE ( 'NONE', *, *, #23983, .T. ) ;
#10362=CARTESIAN_POINT ( 'NONE',  ( -0.02418142828330846830, 0.06026811487149354857, -0.1249999999999999029 ) ) ;
#10641=CARTESIAN_POINT ( 'NONE',  ( 9.860761315262654615E-34, -0.4700000000000001954, 0.04000000000000001471 ) ) ;
#10670=DIRECTION ( 'NONE',  ( 0.000000000000000000, 0.000000000000000000, 1.000000000000000000 ) ) ;
#10722=ORIENTED_EDGE ( 'NONE', *, *, #30058, .F. ) ;
#10761=VECTOR ( 'NONE', #23708, 39.37007874015748143 ) ;
#10768=DIRECTION ( 'NONE',  ( 0.000000000000000000, 0.000000000000000000, 1.000000000000000000 ) ) ;
#10814=FACE_OUTER_BOUND ( 'NONE', #33189, .T. ) ;
#10821=FACE_OUTER_BOUND ( 'NONE', #32913, .T. ) ;
#10846=PRODUCT_DEFINITION_FORMATION_WITH_SPECIFIED_SOURCE ( 'ANY', '', #33451, .NOT_KNOWN. ) ;
#10967=LENGTH_MEASURE_WITH_UNIT ( LENGTH_MEASURE( 0.02539999999999999897 ), #38919 );
#10985=VERTEX_POINT ( 'NONE', #27915 ) ;
#11119=CARTESIAN_POINT ( 'NONE',  ( 0.07216878364870311924, 0.08000000000000023759, 0.1249999999999999029 ) ) ;
#11150=LINE ( 'NONE', #26389, #10761 ) ;
#11166=PRODUCT_DEFINITION ( 'UNKNOWN', '', #10846, #4325 ) ;
#11171=CARTESIAN_POINT ( 'NONE',  ( 0.1202595235781068889, 0.06028806207340008799, -0.04170439506869255686 ) ) ;
#11211=ORIENTED_EDGE ( 'NONE', *, *, #32880, .F. ) ;
#11300=AXIS2_PLACEMENT_3D ( 'NONE', #34194, #22093, #40575 ) ;
#11373=CARTESIAN_POINT ( 'NONE',  ( 0.1443375672974070711, 0.05141091571461162829, 0.000000000000000000 ) ) ;
#11399=( GEOMETRIC_REPRESENTATION_CONTEXT ( 3 ) GLOBAL_UNCERTAINTY_ASSIGNED_CONTEXT ( ( #15737 ) ) GLOBAL_UNIT_ASSIGNED_CONTEXT ( ( #1126, #26195, #23112 ) ) REPRESENTATION_CONTEXT ( 'NONE', 'WORKASPACE' ) );
#11408=SHAPE_DEFINITION_REPRESENTATION ( #17355, #30147 ) ;
#11659=LINE ( 'NONE', #30585, #39562 ) ;
#11688=ORIENTED_EDGE ( 'NONE', *, *, #12008, .F. ) ;
#11834=ORIENTED_EDGE ( 'NONE', *, *, #15702, .F. ) ;
#11962=DIRECTION ( 'NONE',  ( -0.8660254037844387076, -5.423418723394462293E-31, -0.5000000000000001110 ) ) ;
#12008=EDGE_CURVE ( 'NONE', #19840, #37283, #18613, .T. ) ;
#12067=DIRECTION ( 'NONE',  ( 0.8660254037844387076, 5.423418723394460541E-31, 0.5000000000000001110 ) ) ;
#12077=CARTESIAN_POINT ( 'NONE',  ( 0.1023754337098985029, 0.06118878220587092853, 0.07268054736755601153 ) ) ;
#12088=CARTESIAN_POINT ( 'NONE',  ( -3.757258772823647403E-22, 0.06117178301711218014, -0.1249999999999999029 ) ) ;
#12216=CARTESIAN_POINT ( 'NONE',  ( -1.502516396515344672E-15, -0.3899999999999999578, 0.05000000000000055789 ) ) ;
#12307=EDGE_LOOP ( 'NONE', ( #11834, #18249 ) ) ;
#12385=CARTESIAN_POINT ( 'NONE',  ( -0.1443375672974067936, 0.08000000000000023759, 0.000000000000000000 ) ) ;
#12446=LINE ( 'NONE', #15734, #14569 ) ;
#12452=EDGE_CURVE ( 'NONE', #19176, #8492, #33581, .T. ) ;
#12467=CARTESIAN_POINT ( 'NONE',  ( 0.07811717810578562571, 0.05441343863104618900, 0.1146970785768719608 ) ) ;
#12508=VECTOR ( 'NONE', #8429, 39.37007874015748854 ) ;
#12559=AXIS2_PLACEMENT_3D ( 'NONE', #2849, #5729, #34110 ) ;
#12595=ORIENTED_EDGE ( 'NONE', *, *, #28253, .F. ) ;
#12656=FACE_OUTER_BOUND ( 'NONE', #36630, .T. ) ;
#12743=ORIENTED_EDGE ( 'NONE', *, *, #6408, .T. ) ;
#12796=AXIS2_PLACEMENT_3D ( 'NONE', #21624, #24911, #5957 ) ;
#12872=VERTEX_POINT ( 'NONE', #36757 ) ;
#12899=AXIS2_PLACEMENT_3D ( 'NONE', #35252, #22720, #22509 ) ;
#13009=VERTEX_POINT ( 'NONE', #9601 ) ;
#13192=ORIENTED_EDGE ( 'NONE', *, *, #29792, .F. ) ;
#13234=VECTOR ( 'NONE', #9329, 39.37007874015748143 ) ;
#13248=LINE ( 'NONE', #31173, #18454 ) ;
#13370=LINE ( 'NONE', #31896, #15411 ) ;
#13451=CARTESIAN_POINT ( 'NONE',  ( 0.02423924040295103929, 0.06026721965051373003, 0.1249999999999993477 ) ) ;
#13479=AXIS2_PLACEMENT_3D ( 'NONE', #39586, #8331, #20901 ) ;
#13499=CARTESIAN_POINT ( 'NONE',  ( -0.07216878364870257800, 0.08000000000000023759, 0.1249999999999993477 ) ) ;
#13669=B_SPLINE_CURVE_WITH_KNOTS ( 'NONE', 3,
 ( #7680, #20244, #14258, #26821, #11171, #23727, #36255, #11373 ),
 .UNSPECIFIED., .F., .F.,
 ( 4, 2, 2, 4 ),
 ( 2.350980519545030896E-07, 0.001838925622864765559, 0.002758270885271171206, 0.003677616147677576636 ),
 .UNSPECIFIED. ) ;
#13672=AXIS2_PLACEMENT_3D ( 'NONE', #39226, #27079, #39612 ) ;
#13709=ORIENTED_EDGE ( 'NONE', *, *, #23324, .F. ) ;
#13724=PRODUCT_CONTEXT ( 'NONE', #26376, 'mechanical' ) ;
#13860=AXIS2_PLACEMENT_3D ( 'NONE', #1248, #20551, #10670 ) ;
#14033=DIRECTION ( 'NONE',  ( 0.5000000000000001110, -3.759415251443887888E-31, -0.8660254037844385966 ) ) ;
#14258=CARTESIAN_POINT ( 'NONE',  ( 0.09596847297451024938, 0.06113703066755007964, -0.08377772888334847345 ) ) ;
#14345=CARTESIAN_POINT ( 'NONE',  ( 0.000000000000000000, 0.08000000000000023759, 0.000000000000000000 ) ) ;
#14391=ORIENTED_EDGE ( 'NONE', *, *, #14563, .T. ) ;
#14412=CARTESIAN_POINT ( 'NONE',  ( -0.07216878364870250862, 0.000000000000000000, 0.1249999999999993477 ) ) ;
#14434=ADVANCED_FACE ( 'NONE', ( #36518 ), #27058, .T. ) ;
#14563=EDGE_CURVE ( 'NONE', #19176, #32215, #15712, .T. ) ;
#14569=VECTOR ( 'NONE', #21935, 39.37007874015748143 ) ;
#14727=EDGE_CURVE ( 'NONE', #22246, #19176, #9881, .T. ) ;
#14807=ADVANCED_FACE ( 'NONE', ( #35654 ), #7455, .T. ) ;
#15219=VECTOR ( 'NONE', #1500, 39.37007874015748143 ) ;
#15250=DIRECTION ( 'NONE',  ( 0.000000000000000000, 5.978086547377980964E-31, 1.000000000000000000 ) ) ;
#15288=B_SPLINE_CURVE_WITH_KNOTS ( 'NONE', 3,
 ( #29481, #16530, #31964, #13451, #38729, #35040 ),
 .UNSPECIFIED., .F., .F.,
 ( 4, 2, 4 ),
 ( 0.005298961318757118392, 0.006215189799740191909, 0.007131418280723266293 ),
 .UNSPECIFIED. ) ;
#15315=CARTESIAN_POINT ( 'NONE',  ( 0.000000000000000000, -0.4700000000000001954, 0.04000000000000000777 ) ) ;
#15330=CARTESIAN_POINT ( 'NONE',  ( -0.1383891728403244537, 0.05441343863104586287, 0.01030292142312777375 ) ) ;
#15351=FACE_OUTER_BOUND ( 'NONE', #6664, .T. ) ;
#15393=ORIENTED_EDGE ( 'NONE', *, *, #9733, .T. ) ;
#15411=VECTOR ( 'NONE', #25944, 39.37007874015748143 ) ;
#15485=FACE_OUTER_BOUND ( 'NONE', #17211, .T. ) ;
#15576=EDGE_LOOP ( 'NONE', ( #13192, #1019, #10079, #36679 ) ) ;
#15702=EDGE_CURVE ( 'NONE', #25927, #433, #24472, .T. ) ;
#15712=LINE ( 'NONE', #28259, #6242 ) ;
#15734=CARTESIAN_POINT ( 'NONE',  ( -1.496393162519607993E-15, -0.3899999999999999578, -0.04999999999999946848 ) ) ;
#15737=UNCERTAINTY_MEASURE_WITH_UNIT (LENGTH_MEASURE( 1.000000000000000082E-05 ), #1126, 'distance_accuracy_value', 'NONE');
#15891=FACE_OUTER_BOUND ( 'NONE', #25138, .T. ) ;
#15960=CARTESIAN_POINT ( 'NONE',  ( 0.000000000000000000, -0.4700000000000001954, 0.000000000000000000 ) ) ;
#16036=ORIENTED_EDGE ( 'NONE', *, *, #18787, .F. ) ;
#16142=CARTESIAN_POINT ( 'NONE',  ( -0.07811717810578547305, 0.05441343863104623063, -0.1146970785768719608 ) ) ;
#16345=DIRECTION ( 'NONE',  ( -0.5000000000000004441, -4.190823558986626968E-31, -0.8660254037844383745 ) ) ;
#16364=EDGE_LOOP ( 'NONE', ( #22786, #1366, #37515, #11688 ) ) ;
#16376=CARTESIAN_POINT ( 'NONE',  ( -1.502516396515344672E-15, -0.3899999999999999578, 5.463695987328526437E-16 ) ) ;
#16495=CIRCLE ( 'NONE', #13860, 0.04000000000000000777 ) ;
#16530=CARTESIAN_POINT ( 'NONE',  ( 0.06045346506656670837, 0.05436763897581790156, 0.1249999999999993477 ) ) ;
#16531=CIRCLE ( 'NONE', #36231, 0.04000000000000000777 ) ;
#16650=AXIS2_PLACEMENT_3D ( 'NONE', #17829, #30598, #21353 ) ;
#16651=ORIENTED_EDGE ( 'NONE', *, *, #9733, .F. ) ;
#16690=EDGE_LOOP ( 'NONE', ( #26574, #5327, #33094, #31334 ) ) ;
#16742=CARTESIAN_POINT ( 'NONE',  ( -0.1023754337098981698, 0.06118878220587095629, -0.07268054736755635847 ) ) ;
#17200=ORIENTED_EDGE ( 'NONE', *, *, #6408, .F. ) ;
#17211=EDGE_LOOP ( 'NONE', ( #11211, #688, #33523, #6269 ) ) ;
#17338=CARTESIAN_POINT ( 'NONE',  ( -0.07216878364870325802, 0.05141091571461162829, -0.1249999999999999029 ) ) ;
#17355=PRODUCT_DEFINITION_SHAPE ( 'NONE', 'NONE',  #11166 ) ;
#17382=DIRECTION ( 'NONE',  ( 1.000000000000000000, 2.465190328815662439E-32, 0.000000000000000000 ) ) ;
#17499=VERTEX_POINT ( 'NONE', #20175 ) ;
#17795=CARTESIAN_POINT ( 'NONE',  ( -1.502516396515344672E-15, -0.3899999999999999578, 5.463695987328526437E-16 ) ) ;
#17824=B_SPLINE_CURVE_WITH_KNOTS ( 'NONE', 3,
 ( #40619, #21101, #33854, #2781, #6050, #18618, #15330, #5239 ),
 .UNSPECIFIED., .F., .F.,
 ( 4, 2, 2, 4 ),
 ( 2.350980519355055435E-07, 0.001838925622864751681, 0.002758270885271160797, 0.003677616147677569697 ),
 .UNSPECIFIED. ) ;
#17829=CARTESIAN_POINT ( 'NONE',  ( 0.000000000000000000, 0.000000000000000000, 0.000000000000000000 ) ) ;
#17885=LINE ( 'NONE', #39491, #12508 ) ;
#17935=VECTOR ( 'NONE', #14033, 39.37007874015748143 ) ;
#17936=EDGE_CURVE ( 'NONE', #35047, #38442, #24437, .T. ) ;
#18029=DIRECTION ( 'NONE',  ( 2.465190328815661892E-32, 1.000000000000000000, -5.978086547377980964E-31 ) ) ;
#18140=CARTESIAN_POINT ( 'NONE',  ( 0.07216878364870311924, 0.08000000000000023759, 0.1249999999999999029 ) ) ;
#18173=ORIENTED_EDGE ( 'NONE', *, *, #19793, .T. ) ;
#18237=DIRECTION ( 'NONE',  ( 0.000000000000000000, 5.978086547377980964E-31, 1.000000000000000000 ) ) ;
#18246=CARTESIAN_POINT ( 'NONE',  ( 0.08411373178446444887, 0.05688556330967591695, 0.1043107429350861731 ) ) ;
#18249=ORIENTED_EDGE ( 'NONE', *, *, #1156, .F. ) ;
#18287=B_SPLINE_CURVE_WITH_KNOTS ( 'NONE', 3,
 ( #23536, #27213, #20423, #24327, #23718, #36245 ),
 .UNSPECIFIED., .F., .F.,
 ( 4, 2, 4 ),
 ( 0.005049958045009090429, 0.005976456838057345525, 0.006902955631105599753 ),
 .UNSPECIFIED. ) ;
#18321=PLANE ( 'NONE',  #12796 ) ;
#18340=( LENGTH_UNIT ( ) NAMED_UNIT ( * ) SI_UNIT ( $, .METRE. ) );
#18392=ORIENTED_EDGE ( 'NONE', *, *, #25359, .T. ) ;
#18406=CYLINDRICAL_SURFACE ( 'NONE', #3358, 0.05000000000000000971 ) ;
#18454=VECTOR ( 'NONE', #16345, 39.37007874015748143 ) ;
#18537=( NAMED_UNIT ( * ) SI_UNIT ( $, .STERADIAN. ) SOLID_ANGLE_UNIT ( ) );
#18613=CIRCLE ( 'NONE', #16650, 0.05000000000000000971 ) ;
#18614=AXIS2_PLACEMENT_3D ( 'NONE', #14345, #20943, #24646 ) ;
#18618=CARTESIAN_POINT ( 'NONE',  ( -0.1323926191616458248, 0.05688556330967550756, 0.02068925706491315727 ) ) ;
#18658=DIRECTION ( 'NONE',  ( -2.465190328815661892E-32, -1.000000000000000000, -6.656013887802287108E-31 ) ) ;
#18787=EDGE_CURVE ( 'NONE', #8811, #17499, #8615, .T. ) ;
#18799=VECTOR ( 'NONE', #38388, 39.37007874015748143 ) ;
#18857=CARTESIAN_POINT ( 'NONE',  ( 0.07216878364870311924, 0.000000000000000000, 0.1249999999999999029 ) ) ;
#18979=ADVANCED_FACE ( 'NONE', ( #10814 ), #29771, .T. ) ;
#19014=CARTESIAN_POINT ( 'NONE',  ( -0.08411373178446428234, 0.05688556330967591002, -0.1043107429350862841 ) ) ;
#19023=ORIENTED_EDGE ( 'NONE', *, *, #12452, .T. ) ;
#19176=VERTEX_POINT ( 'NONE', #2921 ) ;
#19384=EDGE_LOOP ( 'NONE', ( #38102, #19023, #12743, #30748, #31340 ) ) ;
#19488=LINE ( 'NONE', #25459, #31797 ) ;
#19725=DIRECTION ( 'NONE',  ( -1.000000000000000000, -2.465190328815662439E-32, 0.000000000000000000 ) ) ;
#19793=EDGE_CURVE ( 'NONE', #23947, #28983, #29121, .T. ) ;
#19840=VERTEX_POINT ( 'NONE', #4873 ) ;
#20008=( GEOMETRIC_REPRESENTATION_CONTEXT ( 3 ) GLOBAL_UNCERTAINTY_ASSIGNED_CONTEXT ( ( #24404 ) ) GLOBAL_UNIT_ASSIGNED_CONTEXT ( ( #36843, #21026, #18537 ) ) REPRESENTATION_CONTEXT ( 'NONE', 'WORKASPACE' ) );
#20028=CARTESIAN_POINT ( 'NONE',  ( -3.757258772823647403E-22, 0.06117178301711218014, -0.1249999999999999029 ) ) ;
#20032=DIRECTION ( 'NONE',  ( 2.465190328815661892E-32, 1.000000000000000000, 6.656013887802287108E-31 ) ) ;
#20079=EDGE_LOOP ( 'NONE', ( #10722, #18173, #40412, #6662, #2229, #22227, #12595 ) ) ;
#20081=DIRECTION ( 'NONE',  ( 0.000000000000000000, 0.000000000000000000, -1.000000000000000000 ) ) ;
#20171=CARTESIAN_POINT ( 'NONE',  ( 0.000000000000000000, -0.4700000000000001954, 0.000000000000000000 ) ) ;
#20175=CARTESIAN_POINT ( 'NONE',  ( 0.07216878364870311924, 0.05141091571461162829, 0.1249999999999999029 ) ) ;
#20244=CARTESIAN_POINT ( 'NONE',  ( 0.08402031424619307853, 0.05739311687334415490, -0.1044725468576913618 ) ) ;
#20423=CARTESIAN_POINT ( 'NONE',  ( 0.02423924040295065072, 0.06026721965051347329, -0.1249999999999999029 ) ) ;
#20487=LINE ( 'NONE', #39597, #39038 ) ;
#20488=EDGE_CURVE ( 'NONE', #10985, #32215, #3882, .T. ) ;
#20551=DIRECTION ( 'NONE',  ( -2.465190328815661892E-32, -1.000000000000000000, -6.656013887802287108E-31 ) ) ;
#20901=DIRECTION ( 'NONE',  ( 0.000000000000000000, 0.000000000000000000, 1.000000000000000000 ) ) ;
#20943=DIRECTION ( 'NONE',  ( -2.465190328815661892E-32, -1.000000000000000000, -6.656013887802287108E-31 ) ) ;
#21026=( NAMED_UNIT ( * ) PLANE_ANGLE_UNIT ( ) SI_UNIT ( $, .RADIAN. ) );
#21101=CARTESIAN_POINT ( 'NONE',  ( -0.08402031424619242628, 0.05739311687334405082, 0.1044725468576922639 ) ) ;
#21311=EDGE_CURVE ( 'NONE', #12872, #22246, #17824, .T. ) ;
#21341=PLANE ( 'NONE',  #6224 ) ;
#21353=DIRECTION ( 'NONE',  ( 0.000000000000000000, 5.978086547377981840E-31, 1.000000000000000000 ) ) ;
#21440=AXIS2_PLACEMENT_3D ( 'NONE', #1355, #38976, #17382 ) ;
#21546=PLANE ( 'NONE',  #8870 ) ;
#21624=CARTESIAN_POINT ( 'NONE',  ( -1.502516396515344672E-15, -0.3899999999999999578, 5.463695987328526437E-16 ) ) ;
#21700=DIRECTION ( 'NONE',  ( 0.000000000000000000, 0.000000000000000000, 1.000000000000000000 ) ) ;
#21906=VERTEX_POINT ( 'NONE', #6514 ) ;
#21935=DIRECTION ( 'NONE',  ( 2.465190328815661892E-32, 1.000000000000000000, 6.656013887802287108E-31 ) ) ;
#22003=CARTESIAN_POINT ( 'NONE',  ( -0.01210526301015784831, 0.06117178301711245075, 0.1249999999999993894 ) ) ;
#22093=DIRECTION ( 'NONE',  ( -0.8660254037844384856, 1.232595164407831384E-31, 0.5000000000000004441 ) ) ;
#22116=ADVANCED_BREP_SHAPE_REPRESENTATION ( '', ( #31982, #27819 ), #20008 ) ;
#22143=ORIENTED_EDGE ( 'NONE', *, *, #7708, .F. ) ;
#22227=ORIENTED_EDGE ( 'NONE', *, *, #21311, .F. ) ;
#22246=VERTEX_POINT ( 'NONE', #6667 ) ;
#22307=FACE_OUTER_BOUND ( 'NONE', #20079, .T. ) ;
#22509=DIRECTION ( 'NONE',  ( 0.000000000000000000, 0.000000000000000000, -1.000000000000000000 ) ) ;
#22549=EDGE_CURVE ( 'NONE', #37283, #19840, #33550, .T. ) ;
#22584=LINE ( 'NONE', #28536, #18799 ) ;
#22720=DIRECTION ( 'NONE',  ( -2.465190328815661892E-32, -1.000000000000000000, -6.656013887802287108E-31 ) ) ;
#22786=ORIENTED_EDGE ( 'NONE', *, *, #2098, .F. ) ;
#22910=CARTESIAN_POINT ( 'NONE',  ( -5.117090377708623197E-34, 0.08000000000000023759, -0.08769881541126035851 ) ) ;
#23077=ADVANCED_FACE ( 'NONE', ( #15485 ), #40566, .F. ) ;
#23112=( NAMED_UNIT ( * ) SI_UNIT ( $, .STERADIAN. ) SOLID_ANGLE_UNIT ( ) );
#23201=ORIENTED_EDGE ( 'NONE', *, *, #32880, .T. ) ;
#23324=EDGE_CURVE ( 'NONE', #21906, #13009, #16531, .T. ) ;
#23398=DIMENSIONAL_EXPONENTS ( 1.000000000000000000, 0.000000000000000000, 0.000000000000000000, 0.000000000000000000, 0.000000000000000000, 0.000000000000000000, 0.000000000000000000 ) ;
#23536=CARTESIAN_POINT ( 'NONE',  ( -3.757258772823647403E-22, 0.06117178301711218014, -0.1249999999999999029 ) ) ;
#23708=DIRECTION ( 'NONE',  ( -2.465190328815661892E-32, -1.000000000000000000, -6.656013887802287108E-31 ) ) ;
#23718=CARTESIAN_POINT ( 'NONE',  ( 0.06045346506656550795, 0.05436763897581790156, -0.1249999999999999029 ) ) ;
#23727=CARTESIAN_POINT ( 'NONE',  ( 0.1323926191616460191, 0.05688556330967539654, -0.02068925706491322666 ) ) ;
#23750=ORIENTED_EDGE ( 'NONE', *, *, #34045, .F. ) ;
#23759=CARTESIAN_POINT ( 'NONE',  ( -0.1443375672974067936, 0.08000000000000023759, 0.000000000000000000 ) ) ;
#23905=DIRECTION ( 'NONE',  ( -2.465190328815661892E-32, -1.000000000000000000, -6.656013887802287108E-31 ) ) ;
#23921=VECTOR ( 'NONE', #19725, 39.37007874015748143 ) ;
#23947=VERTEX_POINT ( 'NONE', #29846 ) ;
#23983=EDGE_CURVE ( 'NONE', #17499, #9507, #39299, .T. ) ;
#24004=ORIENTED_EDGE ( 'NONE', *, *, #17936, .F. ) ;
#24075=DIRECTION ( 'NONE',  ( 0.000000000000000000, 0.000000000000000000, 1.000000000000000000 ) ) ;
#24201=DIRECTION ( 'NONE',  ( 2.465190328815661892E-32, 1.000000000000000000, 6.656013887802287108E-31 ) ) ;
#24218=DIRECTION ( 'NONE',  ( -2.465190328815661892E-32, -1.000000000000000000, -6.656013887802287108E-31 ) ) ;
#24292=ORIENTED_EDGE ( 'NONE', *, *, #23983, .F. ) ;
#24300=CARTESIAN_POINT ( 'NONE',  ( 0.000000000000000000, 0.08000000000000023759, 0.000000000000000000 ) ) ;
#24327=CARTESIAN_POINT ( 'NONE',  ( 0.04855986989123495939, 0.05683501216513824755, -0.1249999999999999029 ) ) ;
#24404=UNCERTAINTY_MEASURE_WITH_UNIT (LENGTH_MEASURE( 1.000000000000000082E-05 ), #36843, 'distance_accuracy_value', 'NONE');
#24437=CIRCLE ( 'NONE', #6677, 0.04000000000000000777 ) ;
#24462=AXIS2_PLACEMENT_3D ( 'NONE', #20171, #27360, #24075 ) ;
#24472=CIRCLE ( 'NONE', #6030, 0.05000000000000000971 ) ;
#24646=DIRECTION ( 'NONE',  ( 0.000000000000000000, 0.000000000000000000, 1.000000000000000000 ) ) ;
#24683=CARTESIAN_POINT ( 'NONE',  ( -0.07216878364870250862, 0.05141091571461216952, 0.1249999999999993477 ) ) ;
#24785=EDGE_CURVE ( 'NONE', #3931, #10985, #13248, .T. ) ;
#24911=DIRECTION ( 'NONE',  ( 2.465190328815661892E-32, 1.000000000000000000, -5.978086547377980964E-31 ) ) ;
#24972=LINE ( 'NONE', #15315, #13234 ) ;
#25138=EDGE_LOOP ( 'NONE', ( #28162, #898, #26637, #36686 ) ) ;
#25278=CARTESIAN_POINT ( 'NONE',  ( -0.04828289906928839859, 0.05688126243839979057, 0.1249999999999993894 ) ) ;
#25359=EDGE_CURVE ( 'NONE', #13009, #21906, #16495, .T. ) ;
#25382=CLOSED_SHELL ( 'NONE', ( #14807, #18979, #14434, #30851, #35535, #34089, #9434, #38811, #37285, #23077, #37309, #9124, #39215, #37618, #26775, #4476 ) ) ;
#25453=DIRECTION ( 'NONE',  ( 0.000000000000000000, 0.000000000000000000, 1.000000000000000000 ) ) ;
#25459=CARTESIAN_POINT ( 'NONE',  ( 0.1443375672974070711, 0.07999999999999969635, 0.000000000000000000 ) ) ;
#25642=ORIENTED_EDGE ( 'NONE', *, *, #7554, .F. ) ;
#25716=VERTEX_POINT ( 'NONE', #29746 ) ;
#25751=ORIENTED_EDGE ( 'NONE', *, *, #3328, .F. ) ;
#25927=VERTEX_POINT ( 'NONE', #27292 ) ;
#25944=DIRECTION ( 'NONE',  ( 0.4999999999999997224, 6.656013887802294115E-31, 0.8660254037844388186 ) ) ;
#26060=DIRECTION ( 'NONE',  ( -2.465190328815661892E-32, -1.000000000000000000, -6.656013887802287108E-31 ) ) ;
#26195=( NAMED_UNIT ( * ) PLANE_ANGLE_UNIT ( ) SI_UNIT ( $, .RADIAN. ) );
#26214=ORIENTED_EDGE ( 'NONE', *, *, #20488, .F. ) ;
#26376=APPLICATION_CONTEXT ( 'configuration controlled 3d designs of mechanical parts and assemblies' ) ;
#26389=CARTESIAN_POINT ( 'NONE',  ( -0.07216878364870257800, 0.08000000000000023759, 0.1249999999999993477 ) ) ;
#26439=DIRECTION ( 'NONE',  ( -2.465190328815661892E-32, -1.000000000000000000, -6.656013887802287108E-31 ) ) ;
#26574=ORIENTED_EDGE ( 'NONE', *, *, #15702, .T. ) ;
#26637=ORIENTED_EDGE ( 'NONE', *, *, #29792, .T. ) ;
#26661=PLANE ( 'NONE',  #21440 ) ;
#26664=ORIENTED_EDGE ( 'NONE', *, *, #2205, .T. ) ;
#26775=ADVANCED_FACE ( 'NONE', ( #7796 ), #7990, .T. ) ;
#26821=CARTESIAN_POINT ( 'NONE',  ( 0.1141309172362124369, 0.06118878220587050526, -0.05231945263244261457 ) ) ;
#27058=CYLINDRICAL_SURFACE ( 'NONE', #13479, 0.05000000000000000971 ) ;
#27079=DIRECTION ( 'NONE',  ( 2.465190328815661892E-32, 1.000000000000000000, 6.656013887802287108E-31 ) ) ;
#27207=AXIS2_PLACEMENT_3D ( 'NONE', #13499, #38583, #36102 ) ;
#27213=CARTESIAN_POINT ( 'NONE',  ( 0.01210505692010060280, 0.06117178301711216626, -0.1249999999999998612 ) ) ;
#27217=CARTESIAN_POINT ( 'NONE',  ( 0.000000000000000000, -0.4700000000000001954, 0.000000000000000000 ) ) ;
#27292=CARTESIAN_POINT ( 'NONE',  ( -1.502516396515344672E-15, -0.3899999999999999578, 0.05000000000000055789 ) ) ;
#27341=EDGE_CURVE ( 'NONE', #25716, #10985, #11659, .T. ) ;
#27360=DIRECTION ( 'NONE',  ( 2.465190328815661892E-32, 1.000000000000000000, 6.656013887802287108E-31 ) ) ;
#27390=EDGE_LOOP ( 'NONE', ( #4122, #13709 ) ) ;
#27419=FACE_OUTER_BOUND ( 'NONE', #15576, .T. ) ;
#27700=FACE_BOUND ( 'NONE', #38552, .T. ) ;
#27819=AXIS2_PLACEMENT_3D ( 'NONE', #8920, #2961, #8315 ) ;
#27910=CARTESIAN_POINT ( 'NONE',  ( -0.07216878364870298046, 0.07999999999999969635, -0.1249999999999999029 ) ) ;
#27915=CARTESIAN_POINT ( 'NONE',  ( 0.07216878364870175921, 0.000000000000000000, -0.1249999999999971689 ) ) ;
#28162=ORIENTED_EDGE ( 'NONE', *, *, #27341, .F. ) ;
#28253=EDGE_CURVE ( 'NONE', #4285, #12872, #29426, .T. ) ;
#28259=CARTESIAN_POINT ( 'NONE',  ( -0.07216878364870298046, 0.07999999999999969635, -0.1249999999999999029 ) ) ;
#28435=PLANE ( 'NONE',  #11300 ) ;
#28536=CARTESIAN_POINT ( 'NONE',  ( -0.07216878364870325802, 0.000000000000000000, -0.1249999999999999029 ) ) ;
#28663=EDGE_LOOP ( 'NONE', ( #1100, #31223, #14391, #3537 ) ) ;
#28919=ORIENTED_EDGE ( 'NONE', *, *, #17936, .T. ) ;
#28976=AXIS2_PLACEMENT_3D ( 'NONE', #12385, #31329, #9502 ) ;
#28983=VERTEX_POINT ( 'NONE', #22910 ) ;
#29067=CARTESIAN_POINT ( 'NONE',  ( -0.04828289906928919656, 0.05688126243839940199, -0.1249999999999999029 ) ) ;
#29070=CARTESIAN_POINT ( 'NONE',  ( -0.09624682736800360683, 0.06028806207340060841, -0.08329560493130658272 ) ) ;
#29121=CIRCLE ( 'NONE', #18614, 0.08769881541126034463 ) ;
#29268=EDGE_CURVE ( 'NONE', #25716, #8811, #13669, .T. ) ;
#29426=B_SPLINE_CURVE_WITH_KNOTS ( 'NONE', 3,
 ( #6339, #22003, #37600, #25278, #5733, #24683 ),
 .UNSPECIFIED., .F., .F.,
 ( 4, 2, 4 ),
 ( 0.007131418280723266293, 0.008047662360606964993, 0.008963906440490661959 ),
 .UNSPECIFIED. ) ;
#29481=CARTESIAN_POINT ( 'NONE',  ( 0.07216878364870311924, 0.05141091571461162829, 0.1249999999999999029 ) ) ;
#29716=DIRECTION ( 'NONE',  ( 0.000000000000000000, 0.000000000000000000, -1.000000000000000000 ) ) ;
#29746=CARTESIAN_POINT ( 'NONE',  ( 0.07216878364870175921, 0.05141091571461216952, -0.1249999999999971689 ) ) ;
#29771=CONICAL_SURFACE ( 'NONE', #39594, 0.07506498716826678907, 1.103346454748738825 ) ;
#29792=EDGE_CURVE ( 'NONE', #8811, #3931, #19488, .T. ) ;
#29838=CARTESIAN_POINT ( 'NONE',  ( 4.898587196589415849E-18, -0.4700000000000001954, -0.04000000000000001471 ) ) ;
#29846=CARTESIAN_POINT ( 'NONE',  ( 1.422893940835647384E-17, 0.08000000000000023759, 0.08769881541126035851 ) ) ;
#30058=EDGE_CURVE ( 'NONE', #23947, #4285, #20487, .T. ) ;
#30123=DIRECTION ( 'NONE',  ( 2.465190328815661892E-32, 1.000000000000000000, 6.656013887802287108E-31 ) ) ;
#30147=SHAPE_REPRESENTATION ( 'pulley screw_short', ( #27819 ), #20008 ) ;
#30289=CIRCLE ( 'NONE', #12559, 0.04000000000000000777 ) ;
#30585=CARTESIAN_POINT ( 'NONE',  ( 0.07216878364870298046, 0.08000000000000023759, -0.1249999999999999029 ) ) ;
#30598=DIRECTION ( 'NONE',  ( 2.465190328815661892E-32, 1.000000000000000000, 6.656013887802287108E-31 ) ) ;
#30638=CONICAL_SURFACE ( 'NONE', #12899, 0.07506498716826678907, 1.103346454748738825 ) ;
#30695=DIRECTION ( 'NONE',  ( -0.5000000000000000000, 3.759415251443887013E-31, 0.8660254037844384856 ) ) ;
#30730=LINE ( 'NONE', #39782, #40395 ) ;
#30748=ORIENTED_EDGE ( 'NONE', *, *, #27341, .T. ) ;
#30851=ADVANCED_FACE ( 'NONE', ( #37246, #8441 ), #18321, .F. ) ;
#30885=SHAPE_REPRESENTATION_RELATIONSHIP ( 'NONE' , 'NONE' ,  #30147, #22116 ) ;
#30981=CARTESIAN_POINT ( 'NONE',  ( 0.000000000000000000, 2.989043273688991467E-32, 0.05000000000000000971 ) ) ;
#31127=CARTESIAN_POINT ( 'NONE',  ( 0.07216878364870311924, 0.000000000000000000, 0.1249999999999999029 ) ) ;
#31173=CARTESIAN_POINT ( 'NONE',  ( 0.1443375672974070711, 0.000000000000000000, 0.000000000000000000 ) ) ;
#31223=ORIENTED_EDGE ( 'NONE', *, *, #14727, .T. ) ;
#31306=FACE_OUTER_BOUND ( 'NONE', #36116, .T. ) ;
#31329=DIRECTION ( 'NONE',  ( 0.8660254037844384856, -2.465190328815710609E-32, -0.5000000000000004441 ) ) ;
#31334=ORIENTED_EDGE ( 'NONE', *, *, #3407, .F. ) ;
#31340=ORIENTED_EDGE ( 'NONE', *, *, #20488, .T. ) ;
#31597=CARTESIAN_POINT ( 'NONE',  ( 0.1443375672974070711, 0.05141091571461162829, 0.000000000000000000 ) ) ;
#31747=AXIS2_PLACEMENT_3D ( 'NONE', #18140, #11962, #30695 ) ;
#31754=CARTESIAN_POINT ( 'NONE',  ( -0.1443375672974067936, 0.05141091571461216952, 0.000000000000000000 ) ) ;
#31797=VECTOR ( 'NONE', #35711, 39.37007874015748143 ) ;
#31896=CARTESIAN_POINT ( 'NONE',  ( -0.1443375672974067936, 0.000000000000000000, 0.000000000000000000 ) ) ;
#31964=CARTESIAN_POINT ( 'NONE',  ( 0.04855986989123576431, 0.05683501216513837939, 0.1249999999999993616 ) ) ;
#31982=MANIFOLD_SOLID_BREP ( 'Boss-Extrude3', #25382 ) ;
#32040=CARTESIAN_POINT ( 'NONE',  ( -0.07216878364870325802, 0.000000000000000000, -0.1249999999999999029 ) ) ;
#32069=EDGE_CURVE ( 'NONE', #38442, #35047, #30289, .T. ) ;
#32157=ORIENTED_EDGE ( 'NONE', *, *, #32069, .T. ) ;
#32215=VERTEX_POINT ( 'NONE', #32040 ) ;
#32274=DIMENSIONAL_EXPONENTS ( 1.000000000000000000, 0.000000000000000000, 0.000000000000000000, 0.000000000000000000, 0.000000000000000000, 0.000000000000000000, 0.000000000000000000 ) ;
#32750=LINE ( 'NONE', #1515, #17935 ) ;
#32880=EDGE_CURVE ( 'NONE', #12872, #8583, #11150, .T. ) ;
#32913=EDGE_LOOP ( 'NONE', ( #24292, #37471, #2477, #23201, #26664 ) ) ;
#32991=DIRECTION ( 'NONE',  ( -2.465190328815661892E-32, -1.000000000000000000, -6.656013887802287108E-31 ) ) ;
#33024=DIRECTION ( 'NONE',  ( 1.093267065177649503E-16, -0.4506112020353472136, 0.8927203059190820245 ) ) ;
#33094=ORIENTED_EDGE ( 'NONE', *, *, #22549, .F. ) ;
#33189=EDGE_LOOP ( 'NONE', ( #15393, #1654, #25642, #16036, #4568, #17200, #22143 ) ) ;
#33413=FACE_OUTER_BOUND ( 'NONE', #19384, .T. ) ;
#33451=PRODUCT ( 'pulley screw_short', 'pulley screw_short', '', ( #13724 ) ) ;
#33506=VECTOR ( 'NONE', #35808, 39.37007874015748143 ) ;
#33523=ORIENTED_EDGE ( 'NONE', *, *, #3166, .T. ) ;
#33550=CIRCLE ( 'NONE', #7941, 0.05000000000000000971 ) ;
#33577=AXIS2_PLACEMENT_3D ( 'NONE', #27217, #20032, #10768 ) ;
#33581=B_SPLINE_CURVE_WITH_KNOTS ( 'NONE', 3,
 ( #17338, #38726, #29067, #10362, #39343, #20028 ),
 .UNSPECIFIED., .F., .F.,
 ( 4, 2, 4 ),
 ( 0.003196928911404663034, 0.004123443478206876948, 0.005049958045009090429 ),
 .UNSPECIFIED. ) ;
#33816=LINE ( 'NONE', #12216, #37106 ) ;
#33854=CARTESIAN_POINT ( 'NONE',  ( -0.09596847297450977754, 0.06113703066755011434, 0.08377772888334905632 ) ) ;
#34045=EDGE_CURVE ( 'NONE', #9507, #3931, #32750, .T. ) ;
#34089=ADVANCED_FACE ( 'NONE', ( #27419 ), #74, .F. ) ;
#34110=DIRECTION ( 'NONE',  ( 0.000000000000000000, 0.000000000000000000, -1.000000000000000000 ) ) ;
#34194=CARTESIAN_POINT ( 'NONE',  ( 0.1443375672974070711, 0.07999999999999969635, 0.000000000000000000 ) ) ;
#34883=CARTESIAN_POINT ( 'NONE',  ( 0.1324860366999178474, 0.05739311687334407164, 0.02052745314230711507 ) ) ;
#35040=CARTESIAN_POINT ( 'NONE',  ( 1.530770926392632502E-17, 0.06117178301711245075, 0.1249999999999993477 ) ) ;
#35047=VERTEX_POINT ( 'NONE', #29838 ) ;
#35252=CARTESIAN_POINT ( 'NONE',  ( 0.000000000000000000, 0.08637707520836798714, 0.000000000000000000 ) ) ;
#35442=CARTESIAN_POINT ( 'NONE',  ( -0.07216878364870325802, 0.05141091571461162829, -0.1249999999999999029 ) ) ;
#35535=ADVANCED_FACE ( 'NONE', ( #10821 ), #986, .F. ) ;
#35608=ORIENTED_EDGE ( 'NONE', *, *, #12008, .T. ) ;
#35625=DIRECTION ( 'NONE',  ( 2.465190328815661892E-32, 1.000000000000000000, 6.656013887802287108E-31 ) ) ;
#35654=FACE_OUTER_BOUND ( 'NONE', #39419, .T. ) ;
#35711=DIRECTION ( 'NONE',  ( -2.465190328815661892E-32, -1.000000000000000000, -6.656013887802287108E-31 ) ) ;
#35808=DIRECTION ( 'NONE',  ( -2.465190328815661892E-32, -1.000000000000000000, -6.656013887802287108E-31 ) ) ;
#35836=DIRECTION ( 'NONE',  ( 0.000000000000000000, 5.978086547377981840E-31, 1.000000000000000000 ) ) ;
#36102=DIRECTION ( 'NONE',  ( -1.000000000000000000, -9.860761315262660705E-32, -5.551115123125790098E-17 ) ) ;
#36116=EDGE_LOOP ( 'NONE', ( #16651, #4664 ) ) ;
#36231=AXIS2_PLACEMENT_3D ( 'NONE', #16376, #18658, #25453 ) ;
#36245=CARTESIAN_POINT ( 'NONE',  ( 0.07216878364870175921, 0.05141091571461216952, -0.1249999999999971689 ) ) ;
#36255=CARTESIAN_POINT ( 'NONE',  ( 0.1383891728403247035, 0.05441343863104571715, -0.01030292142312775466 ) ) ;
#36506=AXIS2_PLACEMENT_3D ( 'NONE', #9481, #71, #15250 ) ;
#36518=FACE_OUTER_BOUND ( 'NONE', #16690, .T. ) ;
#36630=EDGE_LOOP ( 'NONE', ( #32157, #28919 ) ) ;
#36679=ORIENTED_EDGE ( 'NONE', *, *, #34045, .T. ) ;
#36686=ORIENTED_EDGE ( 'NONE', *, *, #24785, .T. ) ;
#36725=DIRECTION ( 'NONE',  ( 0.000000000000000000, 0.000000000000000000, 1.000000000000000000 ) ) ;
#36757=CARTESIAN_POINT ( 'NONE',  ( -0.07216878364870250862, 0.05141091571461216952, 0.1249999999999993477 ) ) ;
#36843=( CONVERSION_BASED_UNIT ( 'INCH', #2704 ) LENGTH_UNIT ( ) NAMED_UNIT ( #32274 ) );
#37106=VECTOR ( 'NONE', #30123, 39.37007874015748143 ) ;
#37246=FACE_OUTER_BOUND ( 'NONE', #12307, .T. ) ;
#37283=VERTEX_POINT ( 'NONE', #30981 ) ;
#37285=ADVANCED_FACE ( 'NONE', ( #8974 ), #21546, .F. ) ;
#37309=ADVANCED_FACE ( 'NONE', ( #27700, #15351 ), #21341, .F. ) ;
#37335=VERTEX_POINT ( 'NONE', #2599 ) ;
#37385=ORIENTED_EDGE ( 'NONE', *, *, #32069, .F. ) ;
#37471=ORIENTED_EDGE ( 'NONE', *, *, #7554, .T. ) ;
#37515=ORIENTED_EDGE ( 'NONE', *, *, #3407, .T. ) ;
#37570=CARTESIAN_POINT ( 'NONE',  ( -0.07216878364870250862, 0.000000000000000000, 0.1249999999999993477 ) ) ;
#37600=CARTESIAN_POINT ( 'NONE',  ( -0.02418142828330810401, 0.06026811487149385388, 0.1249999999999993616 ) ) ;
#37618=ADVANCED_FACE ( 'NONE', ( #31306 ), #3517, .T. ) ;
#38102=ORIENTED_EDGE ( 'NONE', *, *, #14563, .F. ) ;
#38223=CIRCLE ( 'NONE', #38861, 0.08769881541126034463 ) ;
#38388=DIRECTION ( 'NONE',  ( -0.5000000000000001110, 4.252453317207020267E-31, 0.8660254037844385966 ) ) ;
#38442=VERTEX_POINT ( 'NONE', #10641 ) ;
#38552=EDGE_LOOP ( 'NONE', ( #8023, #35608 ) ) ;
#38583=DIRECTION ( 'NONE',  ( 5.551115123125790098E-17, -6.347865096700338130E-31, -1.000000000000000000 ) ) ;
#38726=CARTESIAN_POINT ( 'NONE',  ( -0.06034227824829814513, 0.05439570041090458635, -0.1249999999999998612 ) ) ;
#38729=CARTESIAN_POINT ( 'NONE',  ( 0.01210505692010079189, 0.06117178301711245769, 0.1249999999999993477 ) ) ;
#38811=ADVANCED_FACE ( 'NONE', ( #33413 ), #26661, .F. ) ;
#38861=AXIS2_PLACEMENT_3D ( 'NONE', #24300, #23905, #2077 ) ;
#38882=ORIENTED_EDGE ( 'NONE', *, *, #3328, .T. ) ;
#38919=( LENGTH_UNIT ( ) NAMED_UNIT ( * ) SI_UNIT ( $, .METRE. ) );
#38976=DIRECTION ( 'NONE',  ( -1.473712114141921197E-62, 5.978086547377980088E-31, 1.000000000000000000 ) ) ;
#39038=VECTOR ( 'NONE', #33024, 39.37007874015748854 ) ;
#39215=ADVANCED_FACE ( 'NONE', ( #22307 ), #30638, .T. ) ;
#39226=CARTESIAN_POINT ( 'NONE',  ( -1.502516396515344672E-15, -0.3899999999999999578, 5.463695987328526437E-16 ) ) ;
#39299=LINE ( 'NONE', #11119, #33506 ) ;
#39343=CARTESIAN_POINT ( 'NONE',  ( -0.01210526301015805301, 0.06117178301711216626, -0.1249999999999999029 ) ) ;
#39419=EDGE_LOOP ( 'NONE', ( #24004, #38882, #1428, #1238 ) ) ;
#39491=CARTESIAN_POINT ( 'NONE',  ( 0.000000000000000000, 0.08637707520836798714, -0.07506498716826678907 ) ) ;
#39562=VECTOR ( 'NONE', #24218, 39.37007874015748143 ) ;
#39586=CARTESIAN_POINT ( 'NONE',  ( -1.502516396515344672E-15, -0.3899999999999999578, 5.463695987328526437E-16 ) ) ;
#39594=AXIS2_PLACEMENT_3D ( 'NONE', #776, #26060, #20081 ) ;
#39597=CARTESIAN_POINT ( 'NONE',  ( 9.192809626365503817E-18, 0.08637707520836798714, 0.07506498716826678907 ) ) ;
#39601=CARTESIAN_POINT ( 'NONE',  ( -1.496393162519607993E-15, -0.3899999999999999578, -0.04999999999999947542 ) ) ;
#39612=DIRECTION ( 'NONE',  ( 0.000000000000000000, 0.000000000000000000, 1.000000000000000000 ) ) ;
#39782=CARTESIAN_POINT ( 'NONE',  ( 4.898587196589414308E-18, -0.4700000000000001954, -0.04000000000000000777 ) ) ;
#39818=FACE_OUTER_BOUND ( 'NONE', #16364, .T. ) ;
#40395=VECTOR ( 'NONE', #5623, 39.37007874015748143 ) ;
#40412=ORIENTED_EDGE ( 'NONE', *, *, #7708, .T. ) ;
#40417=CARTESIAN_POINT ( 'NONE',  ( -1.502516396515344672E-15, -0.3899999999999999578, 5.463695987328526437E-16 ) ) ;
#40456=AXIS2_PLACEMENT_3D ( 'NONE', #15960, #6888, #4000 ) ;
#40566=PLANE ( 'NONE',  #28976 ) ;
#40575=DIRECTION ( 'NONE',  ( 0.5000000000000003331, 6.162975822039154730E-31, 0.8660254037844383745 ) ) ;
#40619=CARTESIAN_POINT ( 'NONE',  ( -0.07216878364870250862, 0.05141091571461216952, 0.1249999999999993477 ) ) ;
#40695=COLOUR_RGB('Black',0.12,0.14,0.17);
#40696=FILL_AREA_STYLE_COLOUR('',#40695);
#40697=FILL_AREA_STYLE('',(#40696));
#40698=SURFACE_STYLE_FILL_AREA(#40697);
#40699=SURFACE_SIDE_STYLE('',(#40698));
#40700=SURFACE_STYLE_USAGE(.BOTH.,#40699);
#40701=PRESENTATION_STYLE_ASSIGNMENT((#40700));
#40718=STYLED_ITEM('',(#40701),#31982);
#40721=MECHANICAL_DESIGN_GEOMETRIC_PRESENTATION_REPRESENTATION('',(#40718),#11399);
ENDSEC;
END-ISO-10303-21;
